ISO-10303-21;
HEADER;
/* Generated by software containing ST-Developer
 * from STEP Tools, Inc. (www.steptools.com) 
 */

FILE_DESCRIPTION(
/* description */ ('STEP AP214'),
/* implementation_level */ '2;1');

FILE_NAME(
/* name */ 'PRT-TQ-1012-08.step',
/* time_stamp */ '2026-10-07T12:49:37-07:00',
/* author */ (''),
/* organization */ (''),
/* preprocessor_version */ 'ST-DEVELOPER v20.2',
/* originating_system */ 'Autodesk Translation Framework v15.15.0.0',
/* authorisation */ '');

FILE_SCHEMA (('AUTOMOTIVE_DESIGN { 1 0 10303 214 3 1 1 }'));
ENDSEC;

DATA;
#10=MECHANICAL_DESIGN_GEOMETRIC_PRESENTATION_REPRESENTATION('',(#300,#301,#302,#303,#304),#33016);
#179=SPHERICAL_SURFACE('',#10834,5.);
#246=SHAPE_REPRESENTATION_RELATIONSHIP('SRR','None',#33140,#273);
#273=ADVANCED_BREP_SHAPE_REPRESENTATION('',(#331),#33001);
#300=STYLED_ITEM('',(#33289),#9712);
#301=STYLED_ITEM('',(#33289),#9713);
#302=STYLED_ITEM('',(#33289),#9714);
#303=STYLED_ITEM('',(#33289),#9722);
#304=STYLED_ITEM('',(#33288),#331);
#331=MANIFOLD_SOLID_BREP('Body1',#9955);
#391=TOROIDAL_SURFACE('',#10832,8.15,1.);
#517=FACE_BOUND('',#1947,.T.);
#518=FACE_BOUND('',#1949,.T.);
#519=FACE_BOUND('',#1952,.T.);
#918=PLANE('',#10819);
#919=PLANE('',#10821);
#920=PLANE('',#10826);
#921=PLANE('',#10827);
#922=PLANE('',#10828);
#923=PLANE('',#10829);
#924=PLANE('',#10830);
#925=PLANE('',#10831);
#1346=FACE_OUTER_BOUND('',#1945,.T.);
#1347=FACE_OUTER_BOUND('',#1946,.T.);
#1348=FACE_OUTER_BOUND('',#1948,.T.);
#1349=FACE_OUTER_BOUND('',#1950,.T.);
#1350=FACE_OUTER_BOUND('',#1951,.T.);
#1351=FACE_OUTER_BOUND('',#1953,.T.);
#1352=FACE_OUTER_BOUND('',#1954,.T.);
#1353=FACE_OUTER_BOUND('',#1955,.T.);
#1354=FACE_OUTER_BOUND('',#1956,.T.);
#1355=FACE_OUTER_BOUND('',#1957,.T.);
#1356=FACE_OUTER_BOUND('',#1958,.T.);
#1357=FACE_OUTER_BOUND('',#1959,.T.);
#1945=EDGE_LOOP('',(#8082,#8083,#8084,#8085,#8086));
#1946=EDGE_LOOP('',(#8087));
#1947=EDGE_LOOP('',(#8088));
#1948=EDGE_LOOP('',(#8089));
#1949=EDGE_LOOP('',(#8090));
#1950=EDGE_LOOP('',(#8091,#8092,#8093,#8094));
#1951=EDGE_LOOP('',(#8095));
#1952=EDGE_LOOP('',(#8096,#8097,#8098,#8099));
#1953=EDGE_LOOP('',(#8100,#8101,#8102,#8103));
#1954=EDGE_LOOP('',(#8104,#8105,#8106,#8107));
#1955=EDGE_LOOP('',(#8108,#8109,#8110,#8111));
#1956=EDGE_LOOP('',(#8112,#8113,#8114,#8115));
#1957=EDGE_LOOP('',(#8116,#8117,#8118,#8119));
#1958=EDGE_LOOP('',(#8120,#8121,#8122,#8123,#8124));
#1959=EDGE_LOOP('',(#8125));
#2451=CIRCLE('',#10816,9.15);
#2452=CIRCLE('',#10817,9.15);
#2453=CIRCLE('',#10818,9.15);
#2454=CIRCLE('',#10820,6.75);
#2455=CIRCLE('',#10822,8.15);
#2456=CIRCLE('',#10823,3.57071421427142);
#2457=CIRCLE('',#10825,6.75);
#2458=CIRCLE('',#10833,1.);
#3079=LINE('',#27735,#3829);
#3080=LINE('',#27747,#3830);
#3081=LINE('',#27752,#3831);
#3082=LINE('',#27754,#3832);
#3083=LINE('',#27756,#3833);
#3084=LINE('',#27757,#3834);
#3085=LINE('',#27760,#3835);
#3086=LINE('',#27762,#3836);
#3087=LINE('',#27763,#3837);
#3088=LINE('',#27766,#3838);
#3089=LINE('',#27767,#3839);
#3090=LINE('',#27770,#3840);
#3091=LINE('',#27771,#3841);
#3092=LINE('',#27773,#3842);
#3829=VECTOR('',#12814,9.15);
#3830=VECTOR('',#12829,6.75);
#3831=VECTOR('',#12834,1000.);
#3832=VECTOR('',#12835,1000.);
#3833=VECTOR('',#12836,1000.);
#3834=VECTOR('',#12837,1000.);
#3835=VECTOR('',#12840,1000.);
#3836=VECTOR('',#12841,1000.);
#3837=VECTOR('',#12842,1000.);
#3838=VECTOR('',#12845,1000.);
#3839=VECTOR('',#12846,1000.);
#3840=VECTOR('',#12849,1000.);
#3841=VECTOR('',#12850,1000.);
#3842=VECTOR('',#12853,1000.);
#4644=VERTEX_POINT('',#27730);
#4645=VERTEX_POINT('',#27731);
#4646=VERTEX_POINT('',#27734);
#4647=VERTEX_POINT('',#27738);
#4648=VERTEX_POINT('',#27741);
#4649=VERTEX_POINT('',#27743);
#4650=VERTEX_POINT('',#27746);
#4651=VERTEX_POINT('',#27750);
#4652=VERTEX_POINT('',#27751);
#4653=VERTEX_POINT('',#27753);
#4654=VERTEX_POINT('',#27755);
#4655=VERTEX_POINT('',#27759);
#4656=VERTEX_POINT('',#27761);
#4657=VERTEX_POINT('',#27765);
#4658=VERTEX_POINT('',#27769);
#5854=EDGE_CURVE('',#4644,#4645,#2451,.T.);
#5855=EDGE_CURVE('',#4645,#4644,#2452,.T.);
#5856=EDGE_CURVE('',#4644,#4646,#3079,.T.);
#5857=EDGE_CURVE('',#4646,#4646,#2453,.T.);
#5858=EDGE_CURVE('',#4647,#4647,#2454,.T.);
#5859=EDGE_CURVE('',#4648,#4648,#2455,.T.);
#5860=EDGE_CURVE('',#4649,#4649,#2456,.T.);
#5861=EDGE_CURVE('',#4647,#4650,#3080,.T.);
#5862=EDGE_CURVE('',#4650,#4650,#2457,.T.);
#5863=EDGE_CURVE('',#4651,#4652,#3081,.T.);
#5864=EDGE_CURVE('',#4653,#4651,#3082,.T.);
#5865=EDGE_CURVE('',#4654,#4653,#3083,.T.);
#5866=EDGE_CURVE('',#4652,#4654,#3084,.T.);
#5867=EDGE_CURVE('',#4655,#4652,#3085,.T.);
#5868=EDGE_CURVE('',#4656,#4655,#3086,.T.);
#5869=EDGE_CURVE('',#4656,#4651,#3087,.T.);
#5870=EDGE_CURVE('',#4657,#4656,#3088,.T.);
#5871=EDGE_CURVE('',#4657,#4653,#3089,.T.);
#5872=EDGE_CURVE('',#4658,#4657,#3090,.T.);
#5873=EDGE_CURVE('',#4658,#4654,#3091,.T.);
#5874=EDGE_CURVE('',#4655,#4658,#3092,.T.);
#5875=EDGE_CURVE('',#4645,#4648,#2458,.T.);
#8082=ORIENTED_EDGE('',*,*,#5854,.T.);
#8083=ORIENTED_EDGE('',*,*,#5855,.T.);
#8084=ORIENTED_EDGE('',*,*,#5856,.T.);
#8085=ORIENTED_EDGE('',*,*,#5857,.F.);
#8086=ORIENTED_EDGE('',*,*,#5856,.F.);
#8087=ORIENTED_EDGE('',*,*,#5857,.T.);
#8088=ORIENTED_EDGE('',*,*,#5858,.F.);
#8089=ORIENTED_EDGE('',*,*,#5859,.T.);
#8090=ORIENTED_EDGE('',*,*,#5860,.F.);
#8091=ORIENTED_EDGE('',*,*,#5858,.T.);
#8092=ORIENTED_EDGE('',*,*,#5861,.T.);
#8093=ORIENTED_EDGE('',*,*,#5862,.F.);
#8094=ORIENTED_EDGE('',*,*,#5861,.F.);
#8095=ORIENTED_EDGE('',*,*,#5862,.T.);
#8096=ORIENTED_EDGE('',*,*,#5863,.F.);
#8097=ORIENTED_EDGE('',*,*,#5864,.F.);
#8098=ORIENTED_EDGE('',*,*,#5865,.F.);
#8099=ORIENTED_EDGE('',*,*,#5866,.F.);
#8100=ORIENTED_EDGE('',*,*,#5863,.T.);
#8101=ORIENTED_EDGE('',*,*,#5867,.F.);
#8102=ORIENTED_EDGE('',*,*,#5868,.F.);
#8103=ORIENTED_EDGE('',*,*,#5869,.T.);
#8104=ORIENTED_EDGE('',*,*,#5864,.T.);
#8105=ORIENTED_EDGE('',*,*,#5869,.F.);
#8106=ORIENTED_EDGE('',*,*,#5870,.F.);
#8107=ORIENTED_EDGE('',*,*,#5871,.T.);
#8108=ORIENTED_EDGE('',*,*,#5865,.T.);
#8109=ORIENTED_EDGE('',*,*,#5871,.F.);
#8110=ORIENTED_EDGE('',*,*,#5872,.F.);
#8111=ORIENTED_EDGE('',*,*,#5873,.T.);
#8112=ORIENTED_EDGE('',*,*,#5866,.T.);
#8113=ORIENTED_EDGE('',*,*,#5873,.F.);
#8114=ORIENTED_EDGE('',*,*,#5874,.F.);
#8115=ORIENTED_EDGE('',*,*,#5867,.T.);
#8116=ORIENTED_EDGE('',*,*,#5868,.T.);
#8117=ORIENTED_EDGE('',*,*,#5874,.T.);
#8118=ORIENTED_EDGE('',*,*,#5872,.T.);
#8119=ORIENTED_EDGE('',*,*,#5870,.T.);
#8120=ORIENTED_EDGE('',*,*,#5854,.F.);
#8121=ORIENTED_EDGE('',*,*,#5855,.F.);
#8122=ORIENTED_EDGE('',*,*,#5875,.T.);
#8123=ORIENTED_EDGE('',*,*,#5859,.F.);
#8124=ORIENTED_EDGE('',*,*,#5875,.F.);
#8125=ORIENTED_EDGE('',*,*,#5860,.T.);
#9313=CYLINDRICAL_SURFACE('',#10815,9.15);
#9314=CYLINDRICAL_SURFACE('',#10824,6.75);
#9712=ADVANCED_FACE('',(#1346),#9313,.T.);
#9713=ADVANCED_FACE('',(#1347,#517),#918,.T.);
#9714=ADVANCED_FACE('',(#1348,#518),#919,.F.);
#9715=ADVANCED_FACE('',(#1349),#9314,.T.);
#9716=ADVANCED_FACE('',(#1350,#519),#920,.T.);
#9717=ADVANCED_FACE('',(#1351),#921,.F.);
#9718=ADVANCED_FACE('',(#1352),#922,.T.);
#9719=ADVANCED_FACE('',(#1353),#923,.F.);
#9720=ADVANCED_FACE('',(#1354),#924,.T.);
#9721=ADVANCED_FACE('',(#1355),#925,.T.);
#9722=ADVANCED_FACE('',(#1356),#391,.T.);
#9723=ADVANCED_FACE('',(#1357),#179,.F.);
#9955=CLOSED_SHELL('',(#9712,#9713,#9714,#9715,#9716,#9717,#9718,#9719,
#9720,#9721,#9722,#9723));
#10814=AXIS2_PLACEMENT_3D('',#27728,#12806,#12807);
#10815=AXIS2_PLACEMENT_3D('',#27729,#12808,#12809);
#10816=AXIS2_PLACEMENT_3D('',#27732,#12810,#12811);
#10817=AXIS2_PLACEMENT_3D('',#27733,#12812,#12813);
#10818=AXIS2_PLACEMENT_3D('',#27736,#12815,#12816);
#10819=AXIS2_PLACEMENT_3D('',#27737,#12817,#12818);
#10820=AXIS2_PLACEMENT_3D('',#27739,#12819,#12820);
#10821=AXIS2_PLACEMENT_3D('',#27740,#12821,#12822);
#10822=AXIS2_PLACEMENT_3D('',#27742,#12823,#12824);
#10823=AXIS2_PLACEMENT_3D('',#27744,#12825,#12826);
#10824=AXIS2_PLACEMENT_3D('',#27745,#12827,#12828);
#10825=AXIS2_PLACEMENT_3D('',#27748,#12830,#12831);
#10826=AXIS2_PLACEMENT_3D('',#27749,#12832,#12833);
#10827=AXIS2_PLACEMENT_3D('',#27758,#12838,#12839);
#10828=AXIS2_PLACEMENT_3D('',#27764,#12843,#12844);
#10829=AXIS2_PLACEMENT_3D('',#27768,#12847,#12848);
#10830=AXIS2_PLACEMENT_3D('',#27772,#12851,#12852);
#10831=AXIS2_PLACEMENT_3D('',#27774,#12854,#12855);
#10832=AXIS2_PLACEMENT_3D('',#27775,#12856,#12857);
#10833=AXIS2_PLACEMENT_3D('',#27776,#12858,#12859);
#10834=AXIS2_PLACEMENT_3D('',#27777,#12860,#12861);
#12806=DIRECTION('axis',(0.,0.,1.));
#12807=DIRECTION('refdir',(1.,0.,0.));
#12808=DIRECTION('center_axis',(0.,-1.,0.));
#12809=DIRECTION('ref_axis',(0.,0.,-1.));
#12810=DIRECTION('center_axis',(0.,1.,0.));
#12811=DIRECTION('ref_axis',(0.,0.,1.));
#12812=DIRECTION('center_axis',(0.,1.,0.));
#12813=DIRECTION('ref_axis',(0.,0.,1.));
#12814=DIRECTION('',(0.,1.,0.));
#12815=DIRECTION('center_axis',(0.,1.,0.));
#12816=DIRECTION('ref_axis',(0.,0.,1.));
#12817=DIRECTION('center_axis',(0.,1.,0.));
#12818=DIRECTION('ref_axis',(0.,0.,1.));
#12819=DIRECTION('center_axis',(0.,1.,0.));
#12820=DIRECTION('ref_axis',(0.,0.,1.));
#12821=DIRECTION('center_axis',(0.,1.,0.));
#12822=DIRECTION('ref_axis',(0.,0.,1.));
#12823=DIRECTION('center_axis',(0.,-1.,0.));
#12824=DIRECTION('ref_axis',(0.,0.,1.));
#12825=DIRECTION('center_axis',(0.,-1.,0.));
#12826=DIRECTION('ref_axis',(0.,0.,-1.));
#12827=DIRECTION('center_axis',(0.,-1.,0.));
#12828=DIRECTION('ref_axis',(0.,0.,-1.));
#12829=DIRECTION('',(0.,1.,0.));
#12830=DIRECTION('center_axis',(0.,1.,0.));
#12831=DIRECTION('ref_axis',(0.,0.,1.));
#12832=DIRECTION('center_axis',(0.,1.,0.));
#12833=DIRECTION('ref_axis',(0.,0.,1.));
#12834=DIRECTION('',(6.10818125343946E-17,0.,1.));
#12835=DIRECTION('',(-1.,0.,1.12644381556936E-16));
#12836=DIRECTION('',(0.,0.,-1.));
#12837=DIRECTION('',(1.,0.,-1.12644381556936E-16));
#12838=DIRECTION('center_axis',(-1.,0.,6.10818125343946E-17));
#12839=DIRECTION('ref_axis',(6.10818125343946E-17,0.,1.));
#12840=DIRECTION('',(1.58091363932832E-17,0.965925826289068,0.258819045102521));
#12841=DIRECTION('',(6.10818125343946E-17,0.,1.));
#12842=DIRECTION('',(-1.58091363932832E-17,0.965925826289068,-0.258819045102521));
#12843=DIRECTION('center_axis',(1.08806117332204E-16,0.258819045102521,
0.965925826289068));
#12844=DIRECTION('ref_axis',(-2.91545112707301E-17,0.965925826289068,-0.258819045102521));
#12845=DIRECTION('',(-1.,0.,1.12644381556936E-16));
#12846=DIRECTION('',(0.,0.965925826289068,-0.258819045102521));
#12847=DIRECTION('center_axis',(1.,0.,0.));
#12848=DIRECTION('ref_axis',(0.,0.,-1.));
#12849=DIRECTION('',(0.,0.,-1.));
#12850=DIRECTION('',(0.,0.965925826289068,0.258819045102521));
#12851=DIRECTION('center_axis',(-1.08806117332204E-16,0.258819045102521,
-0.965925826289068));
#12852=DIRECTION('ref_axis',(2.91545112707301E-17,0.965925826289068,0.258819045102521));
#12853=DIRECTION('',(1.,0.,-1.12644381556936E-16));
#12854=DIRECTION('center_axis',(0.,1.,0.));
#12855=DIRECTION('ref_axis',(0.,0.,1.));
#12856=DIRECTION('center_axis',(0.,1.,0.));
#12857=DIRECTION('ref_axis',(0.,0.,1.));
#12858=DIRECTION('center_axis',(-1.,0.,1.22464679914735E-16));
#12859=DIRECTION('ref_axis',(-1.22464679914735E-16,0.,-1.));
#12860=DIRECTION('center_axis',(-6.12323399573677E-17,0.,-1.));
#12861=DIRECTION('ref_axis',(-1.,0.,0.));
#27728=CARTESIAN_POINT('',(0.,0.,0.));
#27729=CARTESIAN_POINT('Origin',(0.,26.,0.));
#27730=CARTESIAN_POINT('',(0.,1.,9.15));
#27731=CARTESIAN_POINT('',(-1.12055182121983E-15,1.,-9.15));
#27732=CARTESIAN_POINT('Origin',(0.,1.,0.));
#27733=CARTESIAN_POINT('Origin',(0.,1.,0.));
#27734=CARTESIAN_POINT('',(0.,26.,9.15));
#27735=CARTESIAN_POINT('',(-1.12055182121983E-15,26.,9.15));
#27736=CARTESIAN_POINT('Origin',(0.,26.,0.));
#27737=CARTESIAN_POINT('Origin',(0.,26.,0.));
#27738=CARTESIAN_POINT('',(0.,26.,6.75));
#27739=CARTESIAN_POINT('Origin',(0.,26.,0.));
#27740=CARTESIAN_POINT('Origin',(0.,0.,0.));
#27741=CARTESIAN_POINT('',(-9.98087141305093E-16,0.,-8.15));
#27742=CARTESIAN_POINT('Origin',(0.,0.,0.));
#27743=CARTESIAN_POINT('',(0.,0.,-3.57071421427142));
#27744=CARTESIAN_POINT('Origin',(0.,0.,0.));
#27745=CARTESIAN_POINT('Origin',(0.,27.5,0.));
#27746=CARTESIAN_POINT('',(0.,27.5,6.75));
#27747=CARTESIAN_POINT('',(-8.26636589424463E-16,27.5,6.75));
#27748=CARTESIAN_POINT('Origin',(0.,27.5,0.));
#27749=CARTESIAN_POINT('Origin',(0.,27.5,0.));
#27750=CARTESIAN_POINT('',(-3.85,27.5,-3.81794919243112));
#27751=CARTESIAN_POINT('',(-3.85,27.5,3.81794919243112));
#27752=CARTESIAN_POINT('',(-3.85,27.5,3.55));
#27753=CARTESIAN_POINT('',(3.85,27.5,-3.81794919243112));
#27754=CARTESIAN_POINT('',(-4.30070525597205E-16,27.5,-3.81794919243112));
#27755=CARTESIAN_POINT('',(3.85,27.5,3.81794919243112));
#27756=CARTESIAN_POINT('',(3.85,27.5,3.55));
#27757=CARTESIAN_POINT('',(4.30070525597205E-16,27.5,3.81794919243112));
#27758=CARTESIAN_POINT('Origin',(-3.85,26.5,3.55));
#27759=CARTESIAN_POINT('',(-3.85,26.5,3.55));
#27760=CARTESIAN_POINT('',(-3.85,26.5,3.55));
#27761=CARTESIAN_POINT('',(-3.85,26.5,-3.55));
#27762=CARTESIAN_POINT('',(-3.85,26.5,3.55));
#27763=CARTESIAN_POINT('',(-3.85,26.5,-3.55));
#27764=CARTESIAN_POINT('Origin',(3.85,26.5,-3.55));
#27765=CARTESIAN_POINT('',(3.85,26.5,-3.55));
#27766=CARTESIAN_POINT('',(3.85,26.5,-3.55));
#27767=CARTESIAN_POINT('',(3.85,24.725,-3.07439018343476));
#27768=CARTESIAN_POINT('Origin',(3.85,26.5,3.55));
#27769=CARTESIAN_POINT('',(3.85,26.5,3.55));
#27770=CARTESIAN_POINT('',(3.85,26.5,3.55));
#27771=CARTESIAN_POINT('',(3.85,26.5,3.55));
#27772=CARTESIAN_POINT('Origin',(3.85,26.5,3.55));
#27773=CARTESIAN_POINT('',(3.85,26.5,3.55));
#27774=CARTESIAN_POINT('Origin',(0.,26.5,0.));
#27775=CARTESIAN_POINT('Origin',(0.,1.,0.));
#27776=CARTESIAN_POINT('Origin',(-9.98087141305093E-16,1.,-8.15));
#27777=CARTESIAN_POINT('Origin',(0.,-3.5,0.));
#32969=UNCERTAINTY_MEASURE_WITH_UNIT(LENGTH_MEASURE(0.01),#33017,
'DISTANCE_ACCURACY_VALUE',
'Maximum model space distance between geometric entities at asserted c
onnectivities');
#32984=UNCERTAINTY_MEASURE_WITH_UNIT(LENGTH_MEASURE(0.01),#33017,
'DISTANCE_ACCURACY_VALUE',
'Maximum model space distance between geometric entities at asserted c
onnectivities');
#33001=(
GEOMETRIC_REPRESENTATION_CONTEXT(3)
GLOBAL_UNCERTAINTY_ASSIGNED_CONTEXT((#32969))
GLOBAL_UNIT_ASSIGNED_CONTEXT((#33017,#33019,#33020))
REPRESENTATION_CONTEXT('','3D')
);
#33016=(
GEOMETRIC_REPRESENTATION_CONTEXT(3)
GLOBAL_UNCERTAINTY_ASSIGNED_CONTEXT((#32984))
GLOBAL_UNIT_ASSIGNED_CONTEXT((#33017,#33019,#33020))
REPRESENTATION_CONTEXT('','3D')
);
#33017=(
LENGTH_UNIT()
NAMED_UNIT(*)
SI_UNIT(.MILLI.,.METRE.)
);
#33019=(
NAMED_UNIT(*)
PLANE_ANGLE_UNIT()
SI_UNIT($,.RADIAN.)
);
#33020=(
NAMED_UNIT(*)
SI_UNIT($,.STERADIAN.)
SOLID_ANGLE_UNIT()
);
#33037=SHAPE_DEFINITION_REPRESENTATION(#33076,#33140);
#33076=PRODUCT_DEFINITION_SHAPE('',$,#33172);
#33140=SHAPE_REPRESENTATION('',(#10814),#33001);
#33155=PRODUCT_DEFINITION_CONTEXT('part definition',#33250,'design');
#33172=PRODUCT_DEFINITION(
'P_Torque Wrench_Plunger_PRT-TQ-1012-08_M_Rev01','PRT-TQ-1012-08',#33203,
#33155);
#33203=PRODUCT_DEFINITION_FORMATION('',$,#33268);
#33250=APPLICATION_CONTEXT(
'Core Data for Automotive Mechanical Design Process');
#33251=PRODUCT_CONTEXT('part definition',#33250,'mechanical');
#33268=PRODUCT('P_Torque Wrench_Plunger_PRT-TQ-1012-08_M_Rev01',
'PRT-TQ-1012-08',$,(#33251));
#33288=PRESENTATION_STYLE_ASSIGNMENT((#33295));
#33289=PRESENTATION_STYLE_ASSIGNMENT((#33296));
#33295=SURFACE_STYLE_USAGE(.BOTH.,#33302);
#33296=SURFACE_STYLE_USAGE(.BOTH.,#33303);
#33302=SURFACE_SIDE_STYLE('',(#33309));
#33303=SURFACE_SIDE_STYLE('',(#33310));
#33309=SURFACE_STYLE_FILL_AREA(#33316);
#33310=SURFACE_STYLE_FILL_AREA(#33317);
#33316=FILL_AREA_STYLE('Opaque(192,192,192)',(#33323));
#33317=FILL_AREA_STYLE('Opaque(255,255,255)',(#33324));
#33323=FILL_AREA_STYLE_COLOUR('Opaque(192,192,192)',#33330);
#33324=FILL_AREA_STYLE_COLOUR('Opaque(255,255,255)',#33331);
#33330=COLOUR_RGB('Opaque(192,192,192)', 0.72549020, 0.75294118, 0.79215686);
#33331=COLOUR_RGB('Opaque(255,255,255)', 0.08235294, 0.09019608, 0.10196078);
ENDSEC;
END-ISO-10303-21;
